ISO-10303-21;
HEADER;
/* Generated by software containing ST-Developer
 * from STEP Tools, Inc. (www.steptools.com) 
 */

FILE_DESCRIPTION(
/* description */ ('Bin tilter linkage'),
/* implementation_level */ '2;1');

FILE_NAME(
/* name */ 'Screw thrust collar.step',
/* time_stamp */ '2026-10-28T03:26:24-07:00',
/* author */ (''),
/* organization */ (''),
/* preprocessor_version */ 'ST-DEVELOPER v20.2',
/* originating_system */ 'Autodesk Translation Framework v15.17.0.0',
/* authorisation */ '');

FILE_SCHEMA (('AUTOMOTIVE_DESIGN { 1 0 10303 214 3 1 1 }'));
ENDSEC;

DATA;
#10=MECHANICAL_DESIGN_GEOMETRIC_PRESENTATION_REPRESENTATION('',(#972),#23728);
#752=SHAPE_REPRESENTATION_RELATIONSHIP('SRR','None',#24224,#858);
#858=ADVANCED_BREP_SHAPE_REPRESENTATION('',(#1083),#23724);
#972=STYLED_ITEM('',(#24772),#1083);
#1083=MANIFOLD_SOLID_BREP('Body1',#12505);
#1486=FACE_BOUND('',#3831,.T.);
#1487=FACE_BOUND('',#3833,.T.);
#1882=PLANE('',#15436);
#1883=PLANE('',#15437);
#2652=FACE_OUTER_BOUND('',#3828,.T.);
#2653=FACE_OUTER_BOUND('',#3829,.T.);
#2654=FACE_OUTER_BOUND('',#3830,.T.);
#2655=FACE_OUTER_BOUND('',#3832,.T.);
#3828=EDGE_LOOP('',(#11225,#11226,#11227,#11228));
#3829=EDGE_LOOP('',(#11229,#11230,#11231,#11232));
#3830=EDGE_LOOP('',(#11233));
#3831=EDGE_LOOP('',(#11234));
#3832=EDGE_LOOP('',(#11235));
#3833=EDGE_LOOP('',(#11236));
#4517=LINE('',#23434,#5192);
#4518=LINE('',#23440,#5193);
#5192=VECTOR('',#19654,0.6);
#5193=VECTOR('',#19661,0.9);
#5943=CIRCLE('',#15431,0.6);
#5944=CIRCLE('',#15432,0.6);
#5945=CIRCLE('',#15434,0.9);
#5946=CIRCLE('',#15435,0.9);
#6912=VERTEX_POINT('',#23431);
#6913=VERTEX_POINT('',#23433);
#6914=VERTEX_POINT('',#23437);
#6915=VERTEX_POINT('',#23439);
#8352=EDGE_CURVE('',#6912,#6912,#5943,.T.);
#8353=EDGE_CURVE('',#6912,#6913,#4517,.T.);
#8354=EDGE_CURVE('',#6913,#6913,#5944,.T.);
#8355=EDGE_CURVE('',#6914,#6914,#5945,.T.);
#8356=EDGE_CURVE('',#6914,#6915,#4518,.T.);
#8357=EDGE_CURVE('',#6915,#6915,#5946,.T.);
#11225=ORIENTED_EDGE('',*,*,#8352,.F.);
#11226=ORIENTED_EDGE('',*,*,#8353,.T.);
#11227=ORIENTED_EDGE('',*,*,#8354,.T.);
#11228=ORIENTED_EDGE('',*,*,#8353,.F.);
#11229=ORIENTED_EDGE('',*,*,#8355,.F.);
#11230=ORIENTED_EDGE('',*,*,#8356,.T.);
#11231=ORIENTED_EDGE('',*,*,#8357,.T.);
#11232=ORIENTED_EDGE('',*,*,#8356,.F.);
#11233=ORIENTED_EDGE('',*,*,#8355,.T.);
#11234=ORIENTED_EDGE('',*,*,#8352,.T.);
#11235=ORIENTED_EDGE('',*,*,#8357,.F.);
#11236=ORIENTED_EDGE('',*,*,#8354,.F.);
#11608=CYLINDRICAL_SURFACE('',#15430,0.6);
#11609=CYLINDRICAL_SURFACE('',#15433,0.9);
#12377=ADVANCED_FACE('',(#2652),#11608,.F.);
#12378=ADVANCED_FACE('',(#2653),#11609,.T.);
#12379=ADVANCED_FACE('',(#2654,#1486),#1882,.T.);
#12380=ADVANCED_FACE('',(#2655,#1487),#1883,.F.);
#12505=CLOSED_SHELL('',(#12377,#12378,#12379,#12380));
#15429=AXIS2_PLACEMENT_3D('',#23429,#19648,#19649);
#15430=AXIS2_PLACEMENT_3D('',#23430,#19650,#19651);
#15431=AXIS2_PLACEMENT_3D('',#23432,#19652,#19653);
#15432=AXIS2_PLACEMENT_3D('',#23435,#19655,#19656);
#15433=AXIS2_PLACEMENT_3D('',#23436,#19657,#19658);
#15434=AXIS2_PLACEMENT_3D('',#23438,#19659,#19660);
#15435=AXIS2_PLACEMENT_3D('',#23441,#19662,#19663);
#15436=AXIS2_PLACEMENT_3D('',#23442,#19664,#19665);
#15437=AXIS2_PLACEMENT_3D('',#23443,#19666,#19667);
#19648=DIRECTION('axis',(0.,0.,1.));
#19649=DIRECTION('refdir',(1.,0.,0.));
#19650=DIRECTION('center_axis',(1.,0.,0.));
#19651=DIRECTION('ref_axis',(0.,0.,-1.));
#19652=DIRECTION('center_axis',(-1.,0.,0.));
#19653=DIRECTION('ref_axis',(0.,0.,-1.));
#19654=DIRECTION('',(-1.,0.,0.));
#19655=DIRECTION('center_axis',(-1.,0.,0.));
#19656=DIRECTION('ref_axis',(0.,0.,-1.));
#19657=DIRECTION('center_axis',(1.,0.,0.));
#19658=DIRECTION('ref_axis',(0.,0.,-1.));
#19659=DIRECTION('center_axis',(1.,0.,0.));
#19660=DIRECTION('ref_axis',(0.,0.,-1.));
#19661=DIRECTION('',(-1.,0.,0.));
#19662=DIRECTION('center_axis',(1.,0.,0.));
#19663=DIRECTION('ref_axis',(0.,0.,-1.));
#19664=DIRECTION('center_axis',(1.,0.,0.));
#19665=DIRECTION('ref_axis',(0.,0.,-1.));
#19666=DIRECTION('center_axis',(1.,0.,0.));
#19667=DIRECTION('ref_axis',(0.,0.,-1.));
#23429=CARTESIAN_POINT('',(0.,0.,0.));
#23430=CARTESIAN_POINT('Origin',(-10.2,-4.5,8.));
#23431=CARTESIAN_POINT('',(-10.,-4.5,8.6));
#23432=CARTESIAN_POINT('Origin',(-10.,-4.5,8.));
#23433=CARTESIAN_POINT('',(-10.2,-4.5,8.6));
#23434=CARTESIAN_POINT('',(-10.2,-4.5,8.6));
#23435=CARTESIAN_POINT('Origin',(-10.2,-4.5,8.));
#23436=CARTESIAN_POINT('Origin',(-10.2,-4.5,8.));
#23437=CARTESIAN_POINT('',(-10.,-4.5,8.9));
#23438=CARTESIAN_POINT('Origin',(-10.,-4.5,8.));
#23439=CARTESIAN_POINT('',(-10.2,-4.5,8.9));
#23440=CARTESIAN_POINT('',(-10.2,-4.5,8.9));
#23441=CARTESIAN_POINT('Origin',(-10.2,-4.5,8.));
#23442=CARTESIAN_POINT('Origin',(-10.,-4.5,8.));
#23443=CARTESIAN_POINT('Origin',(-10.2,-4.5,8.));
#23607=UNCERTAINTY_MEASURE_WITH_UNIT(LENGTH_MEASURE(0.001),#23729,
'DISTANCE_ACCURACY_VALUE',
'Maximum model space distance between geometric entities at asserted c
onnectivities');
#23611=UNCERTAINTY_MEASURE_WITH_UNIT(LENGTH_MEASURE(0.001),#23729,
'DISTANCE_ACCURACY_VALUE',
'Maximum model space distance between geometric entities at asserted c
onnectivities');
#23724=(
GEOMETRIC_REPRESENTATION_CONTEXT(3)
GLOBAL_UNCERTAINTY_ASSIGNED_CONTEXT((#23607))
GLOBAL_UNIT_ASSIGNED_CONTEXT((#23729,#23731,#23732))
REPRESENTATION_CONTEXT('','3D')
);
#23728=(
GEOMETRIC_REPRESENTATION_CONTEXT(3)
GLOBAL_UNCERTAINTY_ASSIGNED_CONTEXT((#23611))
GLOBAL_UNIT_ASSIGNED_CONTEXT((#23729,#23731,#23732))
REPRESENTATION_CONTEXT('','3D')
);
#23729=(
LENGTH_UNIT()
NAMED_UNIT(*)
SI_UNIT(.CENTI.,.METRE.)
);
#23731=(
NAMED_UNIT(*)
PLANE_ANGLE_UNIT()
SI_UNIT($,.RADIAN.)
);
#23732=(
NAMED_UNIT(*)
SI_UNIT($,.STERADIAN.)
SOLID_ANGLE_UNIT()
);
#23845=SHAPE_DEFINITION_REPRESENTATION(#24096,#24224);
#24096=PRODUCT_DEFINITION_SHAPE('',$,#24341);
#24224=SHAPE_REPRESENTATION('',(#15429),#23724);
#24228=PRODUCT_DEFINITION_CONTEXT('part definition',#24578,'design');
#24341=PRODUCT_DEFINITION('Screw thrust collar','Screw thrust collar',#24457,
#24228);
#24457=PRODUCT_DEFINITION_FORMATION('',$,#24692);
#24578=APPLICATION_CONTEXT(
'Core Data for Automotive Mechanical Design Process');
#24579=PRODUCT_CONTEXT('part definition',#24578,'mechanical');
#24692=PRODUCT('Screw thrust collar','Screw thrust collar',
'Screw thrust collar',(#24579));
#24766=COLOUR_RGB('Black',0.12,0.14,0.17);
#24767=FILL_AREA_STYLE_COLOUR('',#24766);
#24768=FILL_AREA_STYLE('',(#24767));
#24769=SURFACE_STYLE_FILL_AREA(#24768);
#24770=SURFACE_SIDE_STYLE('',(#24769));
#24771=SURFACE_STYLE_USAGE(.BOTH.,#24770);
#24772=PRESENTATION_STYLE_ASSIGNMENT((#24771));
ENDSEC;
END-ISO-10303-21;
